ISO-10303-21;
HEADER;
/* Generated by software containing ST-Developer
 * from STEP Tools, Inc. (www.steptools.com) 
 */

FILE_DESCRIPTION(
/* description */ (''),
/* implementation_level */ '2;1');

FILE_NAME(
/* name */ 'Back_Block.step',
/* time_stamp */ '2026-10-19T02:00:06+06:00',
/* author */ (''),
/* organization */ (''),
/* preprocessor_version */ 'ST-DEVELOPER v20.2',
/* originating_system */ 'Autodesk Translation Framework v15.15.0.0',
/* authorisation */ '');

FILE_SCHEMA (('AUTOMOTIVE_DESIGN { 1 0 10303 214 3 1 1 }'));
ENDSEC;

DATA;
#10=MECHANICAL_DESIGN_GEOMETRIC_PRESENTATION_REPRESENTATION('',(#115),#4833);
#93=SHAPE_REPRESENTATION_RELATIONSHIP('SRR','None',#4884,#104);
#104=ADVANCED_BREP_SHAPE_REPRESENTATION('',(#126),#4832);
#115=STYLED_ITEM('',(#4971),#126);
#126=MANIFOLD_SOLID_BREP('Back_Block',#2697);
#258=PLANE('',#3069);
#259=PLANE('',#3070);
#260=PLANE('',#3071);
#261=PLANE('',#3072);
#262=PLANE('',#3073);
#263=PLANE('',#3074);
#264=PLANE('',#3075);
#265=PLANE('',#3076);
#266=PLANE('',#3077);
#267=PLANE('',#3078);
#419=FACE_OUTER_BOUND('',#617,.T.);
#420=FACE_OUTER_BOUND('',#618,.T.);
#421=FACE_OUTER_BOUND('',#619,.T.);
#422=FACE_OUTER_BOUND('',#620,.T.);
#423=FACE_OUTER_BOUND('',#621,.T.);
#424=FACE_OUTER_BOUND('',#622,.T.);
#425=FACE_OUTER_BOUND('',#623,.T.);
#426=FACE_OUTER_BOUND('',#624,.T.);
#427=FACE_OUTER_BOUND('',#625,.T.);
#428=FACE_OUTER_BOUND('',#626,.T.);
#617=EDGE_LOOP('',(#2425,#2426,#2427,#2428));
#618=EDGE_LOOP('',(#2429,#2430,#2431,#2432));
#619=EDGE_LOOP('',(#2433,#2434,#2435,#2436,#2437,#2438,#2439,#2440));
#620=EDGE_LOOP('',(#2441,#2442,#2443,#2444));
#621=EDGE_LOOP('',(#2445,#2446,#2447,#2448));
#622=EDGE_LOOP('',(#2449,#2450,#2451,#2452));
#623=EDGE_LOOP('',(#2453,#2454,#2455,#2456));
#624=EDGE_LOOP('',(#2457,#2458,#2459,#2460));
#625=EDGE_LOOP('',(#2461,#2462,#2463,#2464));
#626=EDGE_LOOP('',(#2465,#2466,#2467,#2468,#2469,#2470,#2471,#2472));
#857=LINE('',#4750,#1111);
#858=LINE('',#4752,#1112);
#859=LINE('',#4754,#1113);
#860=LINE('',#4755,#1114);
#861=LINE('',#4758,#1115);
#862=LINE('',#4760,#1116);
#863=LINE('',#4761,#1117);
#864=LINE('',#4764,#1118);
#865=LINE('',#4766,#1119);
#866=LINE('',#4768,#1120);
#867=LINE('',#4770,#1121);
#868=LINE('',#4772,#1122);
#869=LINE('',#4773,#1123);
#870=LINE('',#4776,#1124);
#871=LINE('',#4777,#1125);
#872=LINE('',#4780,#1126);
#873=LINE('',#4781,#1127);
#874=LINE('',#4784,#1128);
#875=LINE('',#4786,#1129);
#876=LINE('',#4787,#1130);
#877=LINE('',#4789,#1131);
#878=LINE('',#4792,#1132);
#879=LINE('',#4793,#1133);
#880=LINE('',#4795,#1134);
#1111=VECTOR('',#3820,10.);
#1112=VECTOR('',#3821,10.);
#1113=VECTOR('',#3822,10.);
#1114=VECTOR('',#3823,10.);
#1115=VECTOR('',#3826,10.);
#1116=VECTOR('',#3827,10.);
#1117=VECTOR('',#3828,10.);
#1118=VECTOR('',#3831,10.);
#1119=VECTOR('',#3832,10.);
#1120=VECTOR('',#3833,10.);
#1121=VECTOR('',#3834,10.);
#1122=VECTOR('',#3835,10.);
#1123=VECTOR('',#3836,10.);
#1124=VECTOR('',#3839,10.);
#1125=VECTOR('',#3840,10.);
#1126=VECTOR('',#3843,10.);
#1127=VECTOR('',#3844,10.);
#1128=VECTOR('',#3847,10.);
#1129=VECTOR('',#3848,10.);
#1130=VECTOR('',#3849,10.);
#1131=VECTOR('',#3852,10.);
#1132=VECTOR('',#3855,10.);
#1133=VECTOR('',#3856,10.);
#1134=VECTOR('',#3859,10.);
#1413=VERTEX_POINT('',#4748);
#1414=VERTEX_POINT('',#4749);
#1415=VERTEX_POINT('',#4751);
#1416=VERTEX_POINT('',#4753);
#1417=VERTEX_POINT('',#4757);
#1418=VERTEX_POINT('',#4759);
#1419=VERTEX_POINT('',#4763);
#1420=VERTEX_POINT('',#4765);
#1421=VERTEX_POINT('',#4767);
#1422=VERTEX_POINT('',#4769);
#1423=VERTEX_POINT('',#4771);
#1424=VERTEX_POINT('',#4775);
#1425=VERTEX_POINT('',#4779);
#1426=VERTEX_POINT('',#4783);
#1427=VERTEX_POINT('',#4785);
#1428=VERTEX_POINT('',#4791);
#1753=EDGE_CURVE('',#1413,#1414,#857,.T.);
#1754=EDGE_CURVE('',#1414,#1415,#858,.T.);
#1755=EDGE_CURVE('',#1415,#1416,#859,.T.);
#1756=EDGE_CURVE('',#1416,#1413,#860,.T.);
#1757=EDGE_CURVE('',#1417,#1414,#861,.T.);
#1758=EDGE_CURVE('',#1418,#1417,#862,.T.);
#1759=EDGE_CURVE('',#1418,#1415,#863,.T.);
#1760=EDGE_CURVE('',#1413,#1419,#864,.T.);
#1761=EDGE_CURVE('',#1420,#1419,#865,.T.);
#1762=EDGE_CURVE('',#1420,#1421,#866,.T.);
#1763=EDGE_CURVE('',#1422,#1421,#867,.T.);
#1764=EDGE_CURVE('',#1422,#1423,#868,.T.);
#1765=EDGE_CURVE('',#1417,#1423,#869,.T.);
#1766=EDGE_CURVE('',#1423,#1424,#870,.T.);
#1767=EDGE_CURVE('',#1424,#1418,#871,.T.);
#1768=EDGE_CURVE('',#1425,#1422,#872,.T.);
#1769=EDGE_CURVE('',#1425,#1424,#873,.T.);
#1770=EDGE_CURVE('',#1419,#1426,#874,.T.);
#1771=EDGE_CURVE('',#1426,#1427,#875,.T.);
#1772=EDGE_CURVE('',#1427,#1420,#876,.T.);
#1773=EDGE_CURVE('',#1416,#1426,#877,.T.);
#1774=EDGE_CURVE('',#1421,#1428,#878,.T.);
#1775=EDGE_CURVE('',#1428,#1425,#879,.T.);
#1776=EDGE_CURVE('',#1427,#1428,#880,.T.);
#2425=ORIENTED_EDGE('',*,*,#1753,.T.);
#2426=ORIENTED_EDGE('',*,*,#1754,.T.);
#2427=ORIENTED_EDGE('',*,*,#1755,.T.);
#2428=ORIENTED_EDGE('',*,*,#1756,.T.);
#2429=ORIENTED_EDGE('',*,*,#1754,.F.);
#2430=ORIENTED_EDGE('',*,*,#1757,.F.);
#2431=ORIENTED_EDGE('',*,*,#1758,.F.);
#2432=ORIENTED_EDGE('',*,*,#1759,.T.);
#2433=ORIENTED_EDGE('',*,*,#1753,.F.);
#2434=ORIENTED_EDGE('',*,*,#1760,.T.);
#2435=ORIENTED_EDGE('',*,*,#1761,.F.);
#2436=ORIENTED_EDGE('',*,*,#1762,.T.);
#2437=ORIENTED_EDGE('',*,*,#1763,.F.);
#2438=ORIENTED_EDGE('',*,*,#1764,.T.);
#2439=ORIENTED_EDGE('',*,*,#1765,.F.);
#2440=ORIENTED_EDGE('',*,*,#1757,.T.);
#2441=ORIENTED_EDGE('',*,*,#1765,.T.);
#2442=ORIENTED_EDGE('',*,*,#1766,.T.);
#2443=ORIENTED_EDGE('',*,*,#1767,.T.);
#2444=ORIENTED_EDGE('',*,*,#1758,.T.);
#2445=ORIENTED_EDGE('',*,*,#1766,.F.);
#2446=ORIENTED_EDGE('',*,*,#1764,.F.);
#2447=ORIENTED_EDGE('',*,*,#1768,.F.);
#2448=ORIENTED_EDGE('',*,*,#1769,.T.);
#2449=ORIENTED_EDGE('',*,*,#1761,.T.);
#2450=ORIENTED_EDGE('',*,*,#1770,.T.);
#2451=ORIENTED_EDGE('',*,*,#1771,.T.);
#2452=ORIENTED_EDGE('',*,*,#1772,.T.);
#2453=ORIENTED_EDGE('',*,*,#1756,.F.);
#2454=ORIENTED_EDGE('',*,*,#1773,.T.);
#2455=ORIENTED_EDGE('',*,*,#1770,.F.);
#2456=ORIENTED_EDGE('',*,*,#1760,.F.);
#2457=ORIENTED_EDGE('',*,*,#1763,.T.);
#2458=ORIENTED_EDGE('',*,*,#1774,.T.);
#2459=ORIENTED_EDGE('',*,*,#1775,.T.);
#2460=ORIENTED_EDGE('',*,*,#1768,.T.);
#2461=ORIENTED_EDGE('',*,*,#1772,.F.);
#2462=ORIENTED_EDGE('',*,*,#1776,.T.);
#2463=ORIENTED_EDGE('',*,*,#1774,.F.);
#2464=ORIENTED_EDGE('',*,*,#1762,.F.);
#2465=ORIENTED_EDGE('',*,*,#1755,.F.);
#2466=ORIENTED_EDGE('',*,*,#1759,.F.);
#2467=ORIENTED_EDGE('',*,*,#1767,.F.);
#2468=ORIENTED_EDGE('',*,*,#1769,.F.);
#2469=ORIENTED_EDGE('',*,*,#1775,.F.);
#2470=ORIENTED_EDGE('',*,*,#1776,.F.);
#2471=ORIENTED_EDGE('',*,*,#1771,.F.);
#2472=ORIENTED_EDGE('',*,*,#1773,.F.);
#2677=ADVANCED_FACE('',(#419),#258,.T.);
#2678=ADVANCED_FACE('',(#420),#259,.T.);
#2679=ADVANCED_FACE('',(#421),#260,.T.);
#2680=ADVANCED_FACE('',(#422),#261,.T.);
#2681=ADVANCED_FACE('',(#423),#262,.T.);
#2682=ADVANCED_FACE('',(#424),#263,.T.);
#2683=ADVANCED_FACE('',(#425),#264,.T.);
#2684=ADVANCED_FACE('',(#426),#265,.T.);
#2685=ADVANCED_FACE('',(#427),#266,.T.);
#2686=ADVANCED_FACE('',(#428),#267,.F.);
#2697=CLOSED_SHELL('',(#2677,#2678,#2679,#2680,#2681,#2682,#2683,#2684,
#2685,#2686));
#3068=AXIS2_PLACEMENT_3D('',#4746,#3816,#3817);
#3069=AXIS2_PLACEMENT_3D('',#4747,#3818,#3819);
#3070=AXIS2_PLACEMENT_3D('',#4756,#3824,#3825);
#3071=AXIS2_PLACEMENT_3D('',#4762,#3829,#3830);
#3072=AXIS2_PLACEMENT_3D('',#4774,#3837,#3838);
#3073=AXIS2_PLACEMENT_3D('',#4778,#3841,#3842);
#3074=AXIS2_PLACEMENT_3D('',#4782,#3845,#3846);
#3075=AXIS2_PLACEMENT_3D('',#4788,#3850,#3851);
#3076=AXIS2_PLACEMENT_3D('',#4790,#3853,#3854);
#3077=AXIS2_PLACEMENT_3D('',#4794,#3857,#3858);
#3078=AXIS2_PLACEMENT_3D('',#4796,#3860,#3861);
#3816=DIRECTION('axis',(0.,0.,1.));
#3817=DIRECTION('refdir',(1.,0.,0.));
#3818=DIRECTION('center_axis',(0.,0.707106781186548,-0.707106781186548));
#3819=DIRECTION('ref_axis',(-1.,0.,0.));
#3820=DIRECTION('',(0.,-0.707106781186548,-0.707106781186548));
#3821=DIRECTION('',(-1.,0.,0.));
#3822=DIRECTION('',(0.,0.707106781186548,0.707106781186548));
#3823=DIRECTION('',(1.,0.,0.));
#3824=DIRECTION('center_axis',(0.,-2.46716227694479E-17,-1.));
#3825=DIRECTION('ref_axis',(0.,1.,-2.46716227694479E-17));
#3826=DIRECTION('',(0.,1.,-2.46716227694479E-17));
#3827=DIRECTION('',(1.,0.,0.));
#3828=DIRECTION('',(0.,1.,-2.46716227694479E-17));
#3829=DIRECTION('center_axis',(1.,0.,0.));
#3830=DIRECTION('ref_axis',(0.,0.,-1.));
#3831=DIRECTION('',(0.,0.,1.));
#3832=DIRECTION('',(0.,0.707106781186548,-0.707106781186548));
#3833=DIRECTION('',(0.,-1.,0.));
#3834=DIRECTION('',(0.,0.707106781186548,0.707106781186548));
#3835=DIRECTION('',(0.,0.,-1.));
#3836=DIRECTION('',(0.,-0.707106781186548,0.707106781186547));
#3837=DIRECTION('center_axis',(0.,-0.707106781186547,-0.707106781186548));
#3838=DIRECTION('ref_axis',(-1.,0.,0.));
#3839=DIRECTION('',(-1.,0.,0.));
#3840=DIRECTION('',(0.,0.707106781186548,-0.707106781186547));
#3841=DIRECTION('center_axis',(0.,-1.,0.));
#3842=DIRECTION('ref_axis',(0.,0.,-1.));
#3843=DIRECTION('',(1.,0.,0.));
#3844=DIRECTION('',(0.,0.,-1.));
#3845=DIRECTION('center_axis',(0.,0.707106781186548,0.707106781186548));
#3846=DIRECTION('ref_axis',(1.,0.,0.));
#3847=DIRECTION('',(-1.,0.,0.));
#3848=DIRECTION('',(0.,-0.707106781186548,0.707106781186548));
#3849=DIRECTION('',(1.,0.,0.));
#3850=DIRECTION('center_axis',(0.,1.,0.));
#3851=DIRECTION('ref_axis',(0.,0.,1.));
#3852=DIRECTION('',(0.,0.,1.));
#3853=DIRECTION('center_axis',(0.,-0.707106781186548,0.707106781186548));
#3854=DIRECTION('ref_axis',(1.,0.,0.));
#3855=DIRECTION('',(-1.,0.,0.));
#3856=DIRECTION('',(0.,-0.707106781186548,-0.707106781186548));
#3857=DIRECTION('center_axis',(0.,0.,1.));
#3858=DIRECTION('ref_axis',(0.,-1.,0.));
#3859=DIRECTION('',(0.,-1.,0.));
#3860=DIRECTION('center_axis',(1.,0.,0.));
#3861=DIRECTION('ref_axis',(0.,1.,0.));
#4746=CARTESIAN_POINT('',(0.,0.,0.));
#4747=CARTESIAN_POINT('Origin',(-110.,87.4999999999895,-17.4999999999979));
#4748=CARTESIAN_POINT('',(-90.,89.9999999999895,-14.9999999999979));
#4749=CARTESIAN_POINT('',(-90.,84.9999999999895,-19.9999999999979));
#4750=CARTESIAN_POINT('',(-90.,69.9999999999895,-34.9999999999979));
#4751=CARTESIAN_POINT('',(-110.,84.9999999999895,-19.9999999999979));
#4752=CARTESIAN_POINT('',(-110.,84.9999999999895,-19.9999999999979));
#4753=CARTESIAN_POINT('',(-110.,89.9999999999895,-14.9999999999979));
#4754=CARTESIAN_POINT('',(-110.,69.9999999999895,-34.9999999999979));
#4755=CARTESIAN_POINT('',(-110.,89.9999999999895,-14.9999999999979));
#4756=CARTESIAN_POINT('Origin',(-110.,-90.0000000000105,-19.9999999999979));
#4757=CARTESIAN_POINT('',(-90.,-85.0000000000105,-19.9999999999979));
#4758=CARTESIAN_POINT('',(-90.,-90.0000000000105,-19.9999999999979));
#4759=CARTESIAN_POINT('',(-110.,-85.0000000000105,-19.9999999999979));
#4760=CARTESIAN_POINT('',(-110.,-85.0000000000105,-19.9999999999979));
#4761=CARTESIAN_POINT('',(-110.,-90.0000000000105,-19.9999999999979));
#4762=CARTESIAN_POINT('Origin',(-90.,-1.05160324892495E-11,2.1138646388863E-12));
#4763=CARTESIAN_POINT('',(-90.,89.9999999999895,15.0000000000021));
#4764=CARTESIAN_POINT('',(-90.,89.9999999999895,-19.9999999999979));
#4765=CARTESIAN_POINT('',(-90.,84.9999999999895,20.0000000000021));
#4766=CARTESIAN_POINT('',(-90.,69.9999999999895,35.0000000000021));
#4767=CARTESIAN_POINT('',(-90.,-85.0000000000105,20.0000000000021));
#4768=CARTESIAN_POINT('',(-90.,89.9999999999895,20.0000000000021));
#4769=CARTESIAN_POINT('',(-90.,-90.0000000000105,15.0000000000021));
#4770=CARTESIAN_POINT('',(-90.,-70.0000000000105,35.0000000000021));
#4771=CARTESIAN_POINT('',(-90.,-90.0000000000105,-14.9999999999979));
#4772=CARTESIAN_POINT('',(-90.,-90.0000000000105,20.0000000000021));
#4773=CARTESIAN_POINT('',(-90.,-70.0000000000105,-34.9999999999979));
#4774=CARTESIAN_POINT('Origin',(-110.,-87.5000000000105,-17.4999999999979));
#4775=CARTESIAN_POINT('',(-110.,-90.0000000000105,-14.9999999999979));
#4776=CARTESIAN_POINT('',(-110.,-90.0000000000105,-14.9999999999979));
#4777=CARTESIAN_POINT('',(-110.,-70.0000000000105,-34.9999999999979));
#4778=CARTESIAN_POINT('Origin',(-110.,-90.0000000000105,20.0000000000021));
#4779=CARTESIAN_POINT('',(-110.,-90.0000000000105,15.0000000000021));
#4780=CARTESIAN_POINT('',(-110.,-90.0000000000105,15.0000000000021));
#4781=CARTESIAN_POINT('',(-110.,-90.0000000000105,20.0000000000021));
#4782=CARTESIAN_POINT('Origin',(-110.,87.4999999999895,17.5000000000021));
#4783=CARTESIAN_POINT('',(-110.,89.9999999999895,15.0000000000021));
#4784=CARTESIAN_POINT('',(-110.,89.9999999999895,15.0000000000021));
#4785=CARTESIAN_POINT('',(-110.,84.9999999999895,20.0000000000021));
#4786=CARTESIAN_POINT('',(-110.,69.9999999999895,35.0000000000021));
#4787=CARTESIAN_POINT('',(-110.,84.9999999999895,20.0000000000021));
#4788=CARTESIAN_POINT('Origin',(-110.,89.9999999999895,-19.9999999999979));
#4789=CARTESIAN_POINT('',(-110.,89.9999999999895,-19.9999999999979));
#4790=CARTESIAN_POINT('Origin',(-110.,-87.5000000000105,17.5000000000021));
#4791=CARTESIAN_POINT('',(-110.,-85.0000000000105,20.0000000000021));
#4792=CARTESIAN_POINT('',(-110.,-85.0000000000105,20.0000000000021));
#4793=CARTESIAN_POINT('',(-110.,-70.0000000000105,35.0000000000021));
#4794=CARTESIAN_POINT('Origin',(-110.,89.9999999999895,20.0000000000021));
#4795=CARTESIAN_POINT('',(-110.,89.9999999999895,20.0000000000021));
#4796=CARTESIAN_POINT('Origin',(-110.,-1.05160324892495E-11,2.11275441586167E-12));
#4819=UNCERTAINTY_MEASURE_WITH_UNIT(LENGTH_MEASURE(0.01),#4834,
'DISTANCE_ACCURACY_VALUE',
'Maximum model space distance between geometric entities at asserted c
onnectivities');
#4820=UNCERTAINTY_MEASURE_WITH_UNIT(LENGTH_MEASURE(0.01),#4834,
'DISTANCE_ACCURACY_VALUE',
'Maximum model space distance between geometric entities at asserted c
onnectivities');
#4832=(
GEOMETRIC_REPRESENTATION_CONTEXT(3)
GLOBAL_UNCERTAINTY_ASSIGNED_CONTEXT((#4819))
GLOBAL_UNIT_ASSIGNED_CONTEXT((#4834,#4836,#4837))
REPRESENTATION_CONTEXT('','3D')
);
#4833=(
GEOMETRIC_REPRESENTATION_CONTEXT(3)
GLOBAL_UNCERTAINTY_ASSIGNED_CONTEXT((#4820))
GLOBAL_UNIT_ASSIGNED_CONTEXT((#4834,#4836,#4837))
REPRESENTATION_CONTEXT('','3D')
);
#4834=(
LENGTH_UNIT()
NAMED_UNIT(*)
SI_UNIT(.MILLI.,.METRE.)
);
#4836=(
NAMED_UNIT(*)
PLANE_ANGLE_UNIT()
SI_UNIT($,.RADIAN.)
);
#4837=(
NAMED_UNIT(*)
SI_UNIT($,.STERADIAN.)
SOLID_ANGLE_UNIT()
);
#4849=SHAPE_DEFINITION_REPRESENTATION(#4861,#4884);
#4861=PRODUCT_DEFINITION_SHAPE('',$,#4897);
#4884=SHAPE_REPRESENTATION('',(#3068),#4832);
#4885=PRODUCT_DEFINITION_CONTEXT('part definition',#4923,'design');
#4897=PRODUCT_DEFINITION('Back_Block','Back_Block',#4909,#4885);
#4909=PRODUCT_DEFINITION_FORMATION('',$,#4936);
#4923=APPLICATION_CONTEXT(
'Core Data for Automotive Mechanical Design Process');
#4924=PRODUCT_CONTEXT('part definition',#4923,'mechanical');
#4936=PRODUCT('Back_Block','Back_Block',$,(#4924));
#4965=COLOUR_RGB('Dark Blue',0.08,0.2,0.34);
#4966=FILL_AREA_STYLE_COLOUR('',#4965);
#4967=FILL_AREA_STYLE('',(#4966));
#4968=SURFACE_STYLE_FILL_AREA(#4967);
#4969=SURFACE_SIDE_STYLE('',(#4968));
#4970=SURFACE_STYLE_USAGE(.BOTH.,#4969);
#4971=PRESENTATION_STYLE_ASSIGNMENT((#4970));
ENDSEC;
END-ISO-10303-21;
